ISO-10303-21;
HEADER;
FILE_DESCRIPTION (('STEP AP203'),
    '1' );
FILE_NAME ('1602p_c_03.step',
    '2026-10-31T14:11:27',
    ( '' ),
    ( '' ),
    'SwSTEP 2.0',
    'SolidWorks 2024',
    '' );
FILE_SCHEMA (( 'AUTOMOTIVE_DESIGN' ));
ENDSEC;

DATA;
#268=CIRCLE ( 'NONE', #7866, 3.499999999999999556 ) ;
#282=ORIENTED_EDGE ( 'NONE', *, *, #4334, .T. ) ;
#411=DIRECTION ( 'NONE',  ( 0.000000000000000000, 0.000000000000000000, -1.000000000000000000 ) ) ;
#415=DIRECTION ( 'NONE',  ( 1.000000000000000000, 0.000000000000000000, 0.000000000000000000 ) ) ;
#448=AXIS2_PLACEMENT_3D ( 'NONE', #2877, #8220, #22687 ) ;
#683=DIRECTION ( 'NONE',  ( -1.000000000000000000, 0.000000000000000000, 0.000000000000000000 ) ) ;
#691=CARTESIAN_POINT ( 'NONE',  ( -17.50000000000000000, -20.00000000000000000, 0.000000000000000000 ) ) ;
#805=DIRECTION ( 'NONE',  ( 0.000000000000000000, -1.000000000000000000, 0.000000000000000000 ) ) ;
#986=VECTOR ( 'NONE', #16074, 1000.000000000000000 ) ;
#1013=AXIS2_PLACEMENT_3D ( 'NONE', #2652, #17386, #9912 ) ;
#1582=EDGE_LOOP ( 'NONE', ( #23157, #15156 ) ) ;
#1963=EDGE_CURVE ( 'NONE', #15512, #7019, #10502, .T. ) ;
#2047=LINE ( 'NONE', #23181, #986 ) ;
#2189=VECTOR ( 'NONE', #21948, 1000.000000000000000 ) ;
#2498=VERTEX_POINT ( 'NONE', #2549 ) ;
#2549=CARTESIAN_POINT ( 'NONE',  ( -17.50000000000000000, -20.00000000000000000, -5.000000000000000000 ) ) ;
#2569=CARTESIAN_POINT ( 'NONE',  ( 0.000000000000000000, 0.000000000000000000, 0.000000000000000000 ) ) ;
#2652=CARTESIAN_POINT ( 'NONE',  ( -20.00000000000000000, -20.00000000000000000, -2.500000000000000000 ) ) ;
#2755=CARTESIAN_POINT ( 'NONE',  ( -20.00000000000000000, -20.00000000000000000, -5.000000000000000000 ) ) ;
#2797=CARTESIAN_POINT ( 'NONE',  ( -20.00000000000000000, -20.00000000000000000, -5.000000000000000000 ) ) ;
#2807=( NAMED_UNIT ( * ) PLANE_ANGLE_UNIT ( ) SI_UNIT ( $, .RADIAN. ) );
#2846=EDGE_CURVE ( 'NONE', #11143, #17128, #2047, .T. ) ;
#2862=DIRECTION ( 'NONE',  ( -1.000000000000000000, 0.000000000000000000, 0.000000000000000000 ) ) ;
#2877=CARTESIAN_POINT ( 'NONE',  ( -20.00000000000000000, -20.00000000000000000, -2.500000000000000000 ) ) ;
#2954=EDGE_LOOP ( 'NONE', ( #14621, #11559 ) ) ;
#2960=ORIENTED_EDGE ( 'NONE', *, *, #11716, .T. ) ;
#2998=CYLINDRICAL_SURFACE ( 'NONE', #1013, 3.499999999999999556 ) ;
#3009=VERTEX_POINT ( 'NONE', #691 ) ;
#3094=ADVANCED_FACE ( 'NONE', ( #18449, #9860 ), #18997, .F. ) ;
#3288=AXIS2_PLACEMENT_3D ( 'NONE', #9766, #4405, #11672 ) ;
#3303=CARTESIAN_POINT ( 'NONE',  ( -23.50000000000000000, -20.00000000000000000, 0.000000000000000000 ) ) ;
#3991=CARTESIAN_POINT ( 'NONE',  ( -23.50000000000000000, -20.00000000000000000, -2.500000000000000000 ) ) ;
#4087=DIRECTION ( 'NONE',  ( -1.000000000000000000, 0.000000000000000000, 0.000000000000000000 ) ) ;
#4200=DIRECTION ( 'NONE',  ( 0.000000000000000000, 0.000000000000000000, 1.000000000000000000 ) ) ;
#4334=EDGE_CURVE ( 'NONE', #3009, #11143, #21340, .T. ) ;
#4391=LINE ( 'NONE', #14719, #2189 ) ;
#4405=DIRECTION ( 'NONE',  ( 0.000000000000000000, 0.000000000000000000, -1.000000000000000000 ) ) ;
#4644=ADVANCED_FACE ( 'NONE', ( #6916 ), #19376, .F. ) ;
#4731=SHAPE_REPRESENTATION ( '1602p_c_03', ( #12739 ), #22192 ) ;
#5544=VERTEX_POINT ( 'NONE', #8258 ) ;
#6191=CARTESIAN_POINT ( 'NONE',  ( -20.00000000000000000, -20.00000000000000000, 0.000000000000000000 ) ) ;
#6207=FACE_OUTER_BOUND ( 'NONE', #11387, .T. ) ;
#6210=CARTESIAN_POINT ( 'NONE',  ( -22.50000000000000000, -20.00000000000000000, 0.000000000000000000 ) ) ;
#6589=CIRCLE ( 'NONE', #22491, 2.499999999999998668 ) ;
#6684=ORIENTED_EDGE ( 'NONE', *, *, #14741, .T. ) ;
#6726=AXIS2_PLACEMENT_3D ( 'NONE', #9418, #20885, #805 ) ;
#6916=FACE_OUTER_BOUND ( 'NONE', #19607, .T. ) ;
#7014=CARTESIAN_POINT ( 'NONE',  ( -16.50000000000000000, -20.00000000000000000, -2.500000000000000000 ) ) ;
#7019=VERTEX_POINT ( 'NONE', #8786 ) ;
#7065=DIRECTION ( 'NONE',  ( -1.000000000000000000, 0.000000000000000000, 0.000000000000000000 ) ) ;
#7443=MECHANICAL_CONTEXT ( 'NONE', #20492, 'mechanical' ) ;
#7548=CARTESIAN_POINT ( 'NONE',  ( -22.50000000000000000, -20.00000000000000000, -5.000000000000000000 ) ) ;
#7623=EDGE_CURVE ( 'NONE', #2498, #17128, #6589, .T. ) ;
#7649=CARTESIAN_POINT ( 'NONE',  ( -20.00000000000000000, -20.00000000000000000, -5.000000000000000000 ) ) ;
#7796=PRODUCT ( '1602p_c_03', '1602p_c_03', '', ( #7443 ) ) ;
#7829=ORIENTED_EDGE ( 'NONE', *, *, #2846, .F. ) ;
#7866=AXIS2_PLACEMENT_3D ( 'NONE', #2755, #20795, #23035 ) ;
#7950=ORIENTED_EDGE ( 'NONE', *, *, #21394, .T. ) ;
#8137=PLANE ( 'NONE',  #18760 ) ;
#8220=DIRECTION ( 'NONE',  ( 0.000000000000000000, 0.000000000000000000, -1.000000000000000000 ) ) ;
#8258=CARTESIAN_POINT ( 'NONE',  ( -16.50000000000000000, -20.00000000000000000, -5.000000000000000000 ) ) ;
#8786=CARTESIAN_POINT ( 'NONE',  ( -16.50000000000000000, -20.00000000000000000, 0.000000000000000000 ) ) ;
#8989=APPLICATION_CONTEXT ( 'configuration controlled 3d designs of mechanical parts and assemblies' ) ;
#9066=EDGE_LOOP ( 'NONE', ( #14400, #2960, #14726, #7829 ) ) ;
#9116=ADVANCED_FACE ( 'NONE', ( #11358, #15364 ), #8137, .T. ) ;
#9418=CARTESIAN_POINT ( 'NONE',  ( -20.00000000000000000, -20.00000000000000000, 0.000000000000000000 ) ) ;
#9625=MANIFOLD_SOLID_BREP ( 'Imported1', #14742 ) ;
#9649=ADVANCED_FACE ( 'NONE', ( #6207 ), #18911, .T. ) ;
#9665=DIRECTION ( 'NONE',  ( -1.000000000000000000, 0.000000000000000000, 0.000000000000000000 ) ) ;
#9766=CARTESIAN_POINT ( 'NONE',  ( -20.00000000000000000, -20.00000000000000000, 0.000000000000000000 ) ) ;
#9860=FACE_OUTER_BOUND ( 'NONE', #2954, .T. ) ;
#9865=ORIENTED_EDGE ( 'NONE', *, *, #7623, .F. ) ;
#9912=DIRECTION ( 'NONE',  ( -1.000000000000000000, 0.000000000000000000, 0.000000000000000000 ) ) ;
#10059=DIRECTION ( 'NONE',  ( 0.000000000000000000, 0.000000000000000000, 1.000000000000000000 ) ) ;
#10082=ORIENTED_EDGE ( 'NONE', *, *, #22989, .T. ) ;
#10502=CIRCLE ( 'NONE', #22976, 3.499999999999999556 ) ;
#10554=PRODUCT_DEFINITION ( 'UNKNOWN', '', #14534, #17536 ) ;
#11074=ORIENTED_EDGE ( 'NONE', *, *, #21964, .T. ) ;
#11143=VERTEX_POINT ( 'NONE', #6210 ) ;
#11240=CARTESIAN_POINT ( 'NONE',  ( -20.00000000000000000, -20.00000000000000000, -2.500000000000000000 ) ) ;
#11263=DIRECTION ( 'NONE',  ( -1.000000000000000000, 0.000000000000000000, 0.000000000000000000 ) ) ;
#11358=FACE_BOUND ( 'NONE', #14066, .T. ) ;
#11387=EDGE_LOOP ( 'NONE', ( #16941, #14994, #6684, #21547 ) ) ;
#11540=CARTESIAN_POINT ( 'NONE',  ( -20.00000000000000000, -20.00000000000000000, -5.000000000000000000 ) ) ;
#11559=ORIENTED_EDGE ( 'NONE', *, *, #21964, .F. ) ;
#11672=DIRECTION ( 'NONE',  ( -1.000000000000000000, 0.000000000000000000, 0.000000000000000000 ) ) ;
#11716=EDGE_CURVE ( 'NONE', #3009, #2498, #4391, .T. ) ;
#12086=( LENGTH_UNIT ( ) NAMED_UNIT ( * ) SI_UNIT ( .MILLI., .METRE. ) );
#12200=SHAPE_REPRESENTATION_RELATIONSHIP ( 'NONE' , 'NONE' ,  #4731, #15041 ) ;
#12225=ORIENTED_EDGE ( 'NONE', *, *, #16957, .F. ) ;
#12243=DIRECTION ( 'NONE',  ( 0.000000000000000000, 0.000000000000000000, -1.000000000000000000 ) ) ;
#12342=ORIENTED_EDGE ( 'NONE', *, *, #21996, .T. ) ;
#12425=ADVANCED_FACE ( 'NONE', ( #20596 ), #20250, .F. ) ;
#12739=AXIS2_PLACEMENT_3D ( 'NONE', #2569, #13380, #415 ) ;
#12945=VERTEX_POINT ( 'NONE', #14977 ) ;
#13159=AXIS2_PLACEMENT_3D ( 'NONE', #20491, #411, #11263 ) ;
#13356=DIRECTION ( 'NONE',  ( 0.000000000000000000, 0.000000000000000000, -1.000000000000000000 ) ) ;
#13380=DIRECTION ( 'NONE',  ( 0.000000000000000000, 0.000000000000000000, 1.000000000000000000 ) ) ;
#13451=CARTESIAN_POINT ( 'NONE',  ( -20.00000000000000000, -20.00000000000000000, -2.500000000000000000 ) ) ;
#14066=EDGE_LOOP ( 'NONE', ( #16502, #18863 ) ) ;
#14115=AXIS2_PLACEMENT_3D ( 'NONE', #18094, #20096, #7065 ) ;
#14183=UNCERTAINTY_MEASURE_WITH_UNIT (LENGTH_MEASURE( 1.000000000000000082E-05 ), #12086, 'distance_accuracy_value', 'NONE');
#14400=ORIENTED_EDGE ( 'NONE', *, *, #4334, .F. ) ;
#14534=PRODUCT_DEFINITION_FORMATION_WITH_SPECIFIED_SOURCE ( 'ANY', '', #7796, .NOT_KNOWN. ) ;
#14591=EDGE_LOOP ( 'NONE', ( #12225, #11074, #12342, #10082 ) ) ;
#14621=ORIENTED_EDGE ( 'NONE', *, *, #1963, .F. ) ;
#14719=CARTESIAN_POINT ( 'NONE',  ( -17.50000000000000000, -20.00000000000000000, -2.500000000000000000 ) ) ;
#14726=ORIENTED_EDGE ( 'NONE', *, *, #18932, .F. ) ;
#14741=EDGE_CURVE ( 'NONE', #5544, #12945, #268, .T. ) ;
#14742=CLOSED_SHELL ( 'NONE', ( #9649, #12425, #4644, #3094, #22562, #9116 ) ) ;
#14889=DIRECTION ( 'NONE',  ( -1.000000000000000000, 0.000000000000000000, 0.000000000000000000 ) ) ;
#14977=CARTESIAN_POINT ( 'NONE',  ( -23.50000000000000000, -20.00000000000000000, -5.000000000000000000 ) ) ;
#14994=ORIENTED_EDGE ( 'NONE', *, *, #16957, .T. ) ;
#15026=LINE ( 'NONE', #3991, #22628 ) ;
#15041=ADVANCED_BREP_SHAPE_REPRESENTATION ( '', ( #9625, #12739 ), #22192 ) ;
#15156=ORIENTED_EDGE ( 'NONE', *, *, #14741, .F. ) ;
#15364=FACE_OUTER_BOUND ( 'NONE', #1582, .T. ) ;
#15512=VERTEX_POINT ( 'NONE', #3303 ) ;
#15815=CIRCLE ( 'NONE', #13159, 3.499999999999999556 ) ;
#15939=AXIS2_PLACEMENT_3D ( 'NONE', #13451, #20221, #9665 ) ;
#16023=CIRCLE ( 'NONE', #20201, 2.499999999999998668 ) ;
#16074=DIRECTION ( 'NONE',  ( 0.000000000000000000, 0.000000000000000000, -1.000000000000000000 ) ) ;
#16502=ORIENTED_EDGE ( 'NONE', *, *, #18932, .T. ) ;
#16870=DIRECTION ( 'NONE',  ( 0.000000000000000000, 0.000000000000000000, -1.000000000000000000 ) ) ;
#16925=SHAPE_DEFINITION_REPRESENTATION ( #20305, #4731 ) ;
#16941=ORIENTED_EDGE ( 'NONE', *, *, #1963, .T. ) ;
#16957=EDGE_CURVE ( 'NONE', #7019, #5544, #17923, .T. ) ;
#17128=VERTEX_POINT ( 'NONE', #7548 ) ;
#17159=ORIENTED_EDGE ( 'NONE', *, *, #2846, .T. ) ;
#17386=DIRECTION ( 'NONE',  ( 0.000000000000000000, 0.000000000000000000, -1.000000000000000000 ) ) ;
#17536=DESIGN_CONTEXT ( 'detailed design', #8989, 'design' ) ;
#17653=( NAMED_UNIT ( * ) SI_UNIT ( $, .STERADIAN. ) SOLID_ANGLE_UNIT ( ) );
#17923=LINE ( 'NONE', #7014, #19842 ) ;
#17989=ORIENTED_EDGE ( 'NONE', *, *, #21394, .F. ) ;
#18094=CARTESIAN_POINT ( 'NONE',  ( -20.00000000000000000, -20.00000000000000000, 0.000000000000000000 ) ) ;
#18426=ORIENTED_EDGE ( 'NONE', *, *, #11716, .F. ) ;
#18449=FACE_BOUND ( 'NONE', #20060, .T. ) ;
#18473=CARTESIAN_POINT ( 'NONE',  ( -20.00000000000000000, -20.00000000000000000, -5.000000000000000000 ) ) ;
#18741=DIRECTION ( 'NONE',  ( 0.000000000000000000, 0.000000000000000000, -1.000000000000000000 ) ) ;
#18760=AXIS2_PLACEMENT_3D ( 'NONE', #18473, #13356, #18830 ) ;
#18800=AXIS2_PLACEMENT_3D ( 'NONE', #11540, #22060, #683 ) ;
#18830=DIRECTION ( 'NONE',  ( 0.000000000000000000, -1.000000000000000000, 0.000000000000000000 ) ) ;
#18863=ORIENTED_EDGE ( 'NONE', *, *, #7623, .T. ) ;
#18911=CYLINDRICAL_SURFACE ( 'NONE', #15939, 3.499999999999999556 ) ;
#18932=EDGE_CURVE ( 'NONE', #17128, #2498, #16023, .T. ) ;
#18997=PLANE ( 'NONE',  #6726 ) ;
#19264=AXIS2_PLACEMENT_3D ( 'NONE', #11240, #20469, #4087 ) ;
#19376=CYLINDRICAL_SURFACE ( 'NONE', #448, 2.499999999999998668 ) ;
#19533=CIRCLE ( 'NONE', #18800, 3.499999999999999556 ) ;
#19607=EDGE_LOOP ( 'NONE', ( #18426, #17989, #17159, #9865 ) ) ;
#19842=VECTOR ( 'NONE', #12243, 1000.000000000000000 ) ;
#20060=EDGE_LOOP ( 'NONE', ( #7950, #282 ) ) ;
#20096=DIRECTION ( 'NONE',  ( 0.000000000000000000, 0.000000000000000000, -1.000000000000000000 ) ) ;
#20201=AXIS2_PLACEMENT_3D ( 'NONE', #2797, #10059, #22143 ) ;
#20221=DIRECTION ( 'NONE',  ( 0.000000000000000000, 0.000000000000000000, -1.000000000000000000 ) ) ;
#20250=CYLINDRICAL_SURFACE ( 'NONE', #19264, 2.499999999999998668 ) ;
#20305=PRODUCT_DEFINITION_SHAPE ( 'NONE', 'NONE',  #10554 ) ;
#20469=DIRECTION ( 'NONE',  ( 0.000000000000000000, 0.000000000000000000, -1.000000000000000000 ) ) ;
#20491=CARTESIAN_POINT ( 'NONE',  ( -20.00000000000000000, -20.00000000000000000, 0.000000000000000000 ) ) ;
#20492=APPLICATION_CONTEXT ( 'configuration controlled 3d designs of mechanical parts and assemblies' ) ;
#20596=FACE_OUTER_BOUND ( 'NONE', #9066, .T. ) ;
#20728=CIRCLE ( 'NONE', #3288, 2.499999999999998668 ) ;
#20795=DIRECTION ( 'NONE',  ( 0.000000000000000000, 0.000000000000000000, 1.000000000000000000 ) ) ;
#20885=DIRECTION ( 'NONE',  ( 0.000000000000000000, 0.000000000000000000, -1.000000000000000000 ) ) ;
#21340=CIRCLE ( 'NONE', #14115, 2.499999999999998668 ) ;
#21394=EDGE_CURVE ( 'NONE', #11143, #3009, #20728, .T. ) ;
#21547=ORIENTED_EDGE ( 'NONE', *, *, #21996, .F. ) ;
#21948=DIRECTION ( 'NONE',  ( 0.000000000000000000, 0.000000000000000000, -1.000000000000000000 ) ) ;
#21964=EDGE_CURVE ( 'NONE', #7019, #15512, #15815, .T. ) ;
#21996=EDGE_CURVE ( 'NONE', #15512, #12945, #15026, .T. ) ;
#22060=DIRECTION ( 'NONE',  ( 0.000000000000000000, 0.000000000000000000, 1.000000000000000000 ) ) ;
#22143=DIRECTION ( 'NONE',  ( -1.000000000000000000, 0.000000000000000000, 0.000000000000000000 ) ) ;
#22192=( GEOMETRIC_REPRESENTATION_CONTEXT ( 3 ) GLOBAL_UNCERTAINTY_ASSIGNED_CONTEXT ( ( #14183 ) ) GLOBAL_UNIT_ASSIGNED_CONTEXT ( ( #12086, #2807, #17653 ) ) REPRESENTATION_CONTEXT ( 'NONE', 'WORKASPACE' ) );
#22481=FACE_OUTER_BOUND ( 'NONE', #14591, .T. ) ;
#22491=AXIS2_PLACEMENT_3D ( 'NONE', #7649, #4200, #14889 ) ;
#22562=ADVANCED_FACE ( 'NONE', ( #22481 ), #2998, .T. ) ;
#22628=VECTOR ( 'NONE', #18741, 1000.000000000000000 ) ;
#22687=DIRECTION ( 'NONE',  ( -1.000000000000000000, 0.000000000000000000, 0.000000000000000000 ) ) ;
#22976=AXIS2_PLACEMENT_3D ( 'NONE', #6191, #16870, #2862 ) ;
#22989=EDGE_CURVE ( 'NONE', #12945, #5544, #19533, .T. ) ;
#23035=DIRECTION ( 'NONE',  ( -1.000000000000000000, 0.000000000000000000, 0.000000000000000000 ) ) ;
#23157=ORIENTED_EDGE ( 'NONE', *, *, #22989, .F. ) ;
#23181=CARTESIAN_POINT ( 'NONE',  ( -22.50000000000000000, -20.00000000000000000, -2.500000000000000000 ) ) ;
#23536=COLOUR_RGB('Slate Gray', 0.40784314, 0.44705882, 0.49803922);
#23537=FILL_AREA_STYLE_COLOUR('',#23536);
#23538=FILL_AREA_STYLE('',(#23537));
#23539=SURFACE_STYLE_FILL_AREA(#23538);
#23540=SURFACE_SIDE_STYLE('',(#23539));
#23541=SURFACE_STYLE_USAGE(.BOTH.,#23540);
#23542=PRESENTATION_STYLE_ASSIGNMENT((#23541));
#23605=STYLED_ITEM('',(#23542),#9625);
#23606=MECHANICAL_DESIGN_GEOMETRIC_PRESENTATION_REPRESENTATION('',(#23605),#22192);
ENDSEC;
END-ISO-10303-21;
